ISO-10303-21;
HEADER;
/* Generated by software containing ST-Developer
 * from STEP Tools, Inc. (www.steptools.com) 
 */

FILE_DESCRIPTION(
/* description */ (''),
/* implementation_level */ '2;1');

FILE_NAME(
/* name */ '16_DIN_6885_A_8x7x16_Parallel_Key.step',
/* time_stamp */ '2026-10-23T00:52:27+05:00',
/* author */ (''),
/* organization */ (''),
/* preprocessor_version */ 'ST-DEVELOPER v20.2',
/* originating_system */ 'Autodesk Translation Framework v15.15.0.0',
/* authorisation */ '');

FILE_SCHEMA (('AUTOMOTIVE_DESIGN { 1 0 10303 214 3 1 1 }'));
ENDSEC;

DATA;
#10=MECHANICAL_DESIGN_GEOMETRIC_PRESENTATION_REPRESENTATION('',(#1552),#59204);
#1512=SHAPE_REPRESENTATION_RELATIONSHIP('SRR','None',#59301,#1532);
#1532=ADVANCED_BREP_SHAPE_REPRESENTATION('',(#1579),#59188);
#1552=STYLED_ITEM('',(#59586),#1579);
#1579=MANIFOLD_SOLID_BREP('Key',#22808);
#1825=PLANE('',#23175);
#1826=PLANE('',#23179);
#1827=PLANE('',#23185);
#1828=PLANE('',#23186);
#1829=PLANE('',#23189);
#1830=PLANE('',#23190);
#2425=CYLINDRICAL_SURFACE('',#23183,0.4);
#2426=CYLINDRICAL_SURFACE('',#23187,0.4);
#2732=FACE_OUTER_BOUND('',#4062,.T.);
#2733=FACE_OUTER_BOUND('',#4063,.T.);
#2734=FACE_OUTER_BOUND('',#4064,.T.);
#2735=FACE_OUTER_BOUND('',#4065,.T.);
#2736=FACE_OUTER_BOUND('',#4066,.T.);
#2737=FACE_OUTER_BOUND('',#4067,.T.);
#2738=FACE_OUTER_BOUND('',#4068,.T.);
#2739=FACE_OUTER_BOUND('',#4069,.T.);
#2740=FACE_OUTER_BOUND('',#4070,.T.);
#2741=FACE_OUTER_BOUND('',#4071,.T.);
#4062=EDGE_LOOP('',(#14936,#14937,#14938,#14939));
#4063=EDGE_LOOP('',(#14940,#14941,#14942,#14943));
#4064=EDGE_LOOP('',(#14944,#14945,#14946,#14947));
#4065=EDGE_LOOP('',(#14948,#14949,#14950,#14951));
#4066=EDGE_LOOP('',(#14952,#14953,#14954,#14955));
#4067=EDGE_LOOP('',(#14956,#14957,#14958,#14959));
#4068=EDGE_LOOP('',(#14960,#14961,#14962,#14963));
#4069=EDGE_LOOP('',(#14964,#14965,#14966,#14967));
#4070=EDGE_LOOP('',(#14968,#14969,#14970,#14971));
#4071=EDGE_LOOP('',(#14972,#14973,#14974,#14975));
#5548=LINE('',#32189,#6981);
#5549=LINE('',#32191,#6982);
#5550=LINE('',#32193,#6983);
#5551=LINE('',#32194,#6984);
#5552=LINE('',#32198,#6985);
#5553=LINE('',#32204,#6986);
#5554=LINE('',#32205,#6987);
#5555=LINE('',#32206,#6988);
#5556=LINE('',#32212,#6989);
#5557=LINE('',#32215,#6990);
#5558=LINE('',#32218,#6991);
#5559=LINE('',#32219,#6992);
#5560=LINE('',#32223,#6993);
#5561=LINE('',#32226,#6994);
#6981=VECTOR('',#25436,1.);
#6982=VECTOR('',#25437,1.);
#6983=VECTOR('',#25438,1.);
#6984=VECTOR('',#25439,1.);
#6985=VECTOR('',#25442,1.);
#6986=VECTOR('',#25449,1.);
#6987=VECTOR('',#25450,1.);
#6988=VECTOR('',#25451,1.);
#6989=VECTOR('',#25460,1.);
#6990=VECTOR('',#25463,1.);
#6991=VECTOR('',#25466,1.);
#6992=VECTOR('',#25467,1.);
#6993=VECTOR('',#25472,1.);
#6994=VECTOR('',#25477,1.);
#8421=CIRCLE('',#23177,0.37);
#8422=CIRCLE('',#23178,0.4);
#8423=CIRCLE('',#23181,0.37);
#8424=CIRCLE('',#23182,0.4);
#8425=CIRCLE('',#23184,0.4);
#8426=CIRCLE('',#23188,0.4);
#9275=VERTEX_POINT('',#32187);
#9276=VERTEX_POINT('',#32188);
#9277=VERTEX_POINT('',#32190);
#9278=VERTEX_POINT('',#32192);
#9279=VERTEX_POINT('',#32196);
#9280=VERTEX_POINT('',#32197);
#9281=VERTEX_POINT('',#32202);
#9282=VERTEX_POINT('',#32203);
#9283=VERTEX_POINT('',#32211);
#9284=VERTEX_POINT('',#32213);
#9285=VERTEX_POINT('',#32217);
#9286=VERTEX_POINT('',#32222);
#11472=EDGE_CURVE('',#9275,#9276,#5548,.T.);
#11473=EDGE_CURVE('',#9276,#9277,#5549,.T.);
#11474=EDGE_CURVE('',#9277,#9278,#5550,.T.);
#11475=EDGE_CURVE('',#9278,#9275,#5551,.T.);
#11476=EDGE_CURVE('',#9279,#9280,#5552,.T.);
#11477=EDGE_CURVE('',#9280,#9276,#8421,.T.);
#11478=EDGE_CURVE('',#9275,#9279,#8422,.T.);
#11479=EDGE_CURVE('',#9281,#9282,#5553,.T.);
#11480=EDGE_CURVE('',#9282,#9280,#5554,.T.);
#11481=EDGE_CURVE('',#9279,#9281,#5555,.T.);
#11482=EDGE_CURVE('',#9277,#9282,#8423,.T.);
#11483=EDGE_CURVE('',#9281,#9278,#8424,.T.);
#11484=EDGE_CURVE('',#9283,#9275,#5556,.T.);
#11485=EDGE_CURVE('',#9283,#9284,#8425,.T.);
#11486=EDGE_CURVE('',#9284,#9279,#5557,.T.);
#11487=EDGE_CURVE('',#9285,#9278,#5558,.T.);
#11488=EDGE_CURVE('',#9283,#9285,#5559,.T.);
#11489=EDGE_CURVE('',#9286,#9281,#5560,.T.);
#11490=EDGE_CURVE('',#9286,#9285,#8426,.T.);
#11491=EDGE_CURVE('',#9286,#9284,#5561,.T.);
#14936=ORIENTED_EDGE('',*,*,#11472,.T.);
#14937=ORIENTED_EDGE('',*,*,#11473,.T.);
#14938=ORIENTED_EDGE('',*,*,#11474,.T.);
#14939=ORIENTED_EDGE('',*,*,#11475,.T.);
#14940=ORIENTED_EDGE('',*,*,#11476,.T.);
#14941=ORIENTED_EDGE('',*,*,#11477,.T.);
#14942=ORIENTED_EDGE('',*,*,#11472,.F.);
#14943=ORIENTED_EDGE('',*,*,#11478,.T.);
#14944=ORIENTED_EDGE('',*,*,#11479,.T.);
#14945=ORIENTED_EDGE('',*,*,#11480,.T.);
#14946=ORIENTED_EDGE('',*,*,#11476,.F.);
#14947=ORIENTED_EDGE('',*,*,#11481,.T.);
#14948=ORIENTED_EDGE('',*,*,#11474,.F.);
#14949=ORIENTED_EDGE('',*,*,#11482,.T.);
#14950=ORIENTED_EDGE('',*,*,#11479,.F.);
#14951=ORIENTED_EDGE('',*,*,#11483,.T.);
#14952=ORIENTED_EDGE('',*,*,#11478,.F.);
#14953=ORIENTED_EDGE('',*,*,#11484,.F.);
#14954=ORIENTED_EDGE('',*,*,#11485,.T.);
#14955=ORIENTED_EDGE('',*,*,#11486,.T.);
#14956=ORIENTED_EDGE('',*,*,#11475,.F.);
#14957=ORIENTED_EDGE('',*,*,#11487,.F.);
#14958=ORIENTED_EDGE('',*,*,#11488,.F.);
#14959=ORIENTED_EDGE('',*,*,#11484,.T.);
#14960=ORIENTED_EDGE('',*,*,#11473,.F.);
#14961=ORIENTED_EDGE('',*,*,#11477,.F.);
#14962=ORIENTED_EDGE('',*,*,#11480,.F.);
#14963=ORIENTED_EDGE('',*,*,#11482,.F.);
#14964=ORIENTED_EDGE('',*,*,#11483,.F.);
#14965=ORIENTED_EDGE('',*,*,#11489,.F.);
#14966=ORIENTED_EDGE('',*,*,#11490,.T.);
#14967=ORIENTED_EDGE('',*,*,#11487,.T.);
#14968=ORIENTED_EDGE('',*,*,#11481,.F.);
#14969=ORIENTED_EDGE('',*,*,#11486,.F.);
#14970=ORIENTED_EDGE('',*,*,#11491,.F.);
#14971=ORIENTED_EDGE('',*,*,#11489,.T.);
#14972=ORIENTED_EDGE('',*,*,#11485,.F.);
#14973=ORIENTED_EDGE('',*,*,#11488,.T.);
#14974=ORIENTED_EDGE('',*,*,#11490,.F.);
#14975=ORIENTED_EDGE('',*,*,#11491,.T.);
#21342=CONICAL_SURFACE('',#23176,0.385,0.785398163397448);
#21343=CONICAL_SURFACE('',#23180,0.385,0.785398163397448);
#21562=ADVANCED_FACE('',(#2732),#1825,.T.);
#21563=ADVANCED_FACE('',(#2733),#21342,.T.);
#21564=ADVANCED_FACE('',(#2734),#1826,.T.);
#21565=ADVANCED_FACE('',(#2735),#21343,.T.);
#21566=ADVANCED_FACE('',(#2736),#2425,.T.);
#21567=ADVANCED_FACE('',(#2737),#1827,.T.);
#21568=ADVANCED_FACE('',(#2738),#1828,.T.);
#21569=ADVANCED_FACE('',(#2739),#2426,.T.);
#21570=ADVANCED_FACE('',(#2740),#1829,.T.);
#21571=ADVANCED_FACE('',(#2741),#1830,.F.);
#22808=CLOSED_SHELL('',(#21562,#21563,#21564,#21565,#21566,#21567,#21568,
#21569,#21570,#21571));
#23174=AXIS2_PLACEMENT_3D('',#32185,#25432,#25433);
#23175=AXIS2_PLACEMENT_3D('',#32186,#25434,#25435);
#23176=AXIS2_PLACEMENT_3D('',#32195,#25440,#25441);
#23177=AXIS2_PLACEMENT_3D('',#32199,#25443,#25444);
#23178=AXIS2_PLACEMENT_3D('',#32200,#25445,#25446);
#23179=AXIS2_PLACEMENT_3D('',#32201,#25447,#25448);
#23180=AXIS2_PLACEMENT_3D('',#32207,#25452,#25453);
#23181=AXIS2_PLACEMENT_3D('',#32208,#25454,#25455);
#23182=AXIS2_PLACEMENT_3D('',#32209,#25456,#25457);
#23183=AXIS2_PLACEMENT_3D('',#32210,#25458,#25459);
#23184=AXIS2_PLACEMENT_3D('',#32214,#25461,#25462);
#23185=AXIS2_PLACEMENT_3D('',#32216,#25464,#25465);
#23186=AXIS2_PLACEMENT_3D('',#32220,#25468,#25469);
#23187=AXIS2_PLACEMENT_3D('',#32221,#25470,#25471);
#23188=AXIS2_PLACEMENT_3D('',#32224,#25473,#25474);
#23189=AXIS2_PLACEMENT_3D('',#32225,#25475,#25476);
#23190=AXIS2_PLACEMENT_3D('',#32227,#25478,#25479);
#25432=DIRECTION('axis',(0.,0.,1.));
#25433=DIRECTION('refdir',(1.,0.,0.));
#25434=DIRECTION('center_axis',(0.707106781186548,0.707106781186548,0.));
#25435=DIRECTION('ref_axis',(0.,0.,-1.));
#25436=DIRECTION('',(0.707106781186548,-0.707106781186548,0.));
#25437=DIRECTION('',(0.,0.,-1.));
#25438=DIRECTION('',(-0.707106781186548,0.707106781186548,0.));
#25439=DIRECTION('',(0.,0.,1.));
#25440=DIRECTION('center_axis',(-1.,0.,0.));
#25441=DIRECTION('ref_axis',(0.,1.,2.77555756156289E-16));
#25442=DIRECTION('',(0.707106781186548,0.707106781186548,0.));
#25443=DIRECTION('center_axis',(-1.,0.,0.));
#25444=DIRECTION('ref_axis',(0.,1.,2.77555756156289E-16));
#25445=DIRECTION('center_axis',(1.,0.,0.));
#25446=DIRECTION('ref_axis',(0.,1.,2.77555756156289E-16));
#25447=DIRECTION('center_axis',(0.707106781186548,-0.707106781186548,0.));
#25448=DIRECTION('ref_axis',(0.,0.,-1.));
#25449=DIRECTION('',(0.707106781186548,0.707106781186548,0.));
#25450=DIRECTION('',(0.,0.,1.));
#25451=DIRECTION('',(0.,0.,-1.));
#25452=DIRECTION('center_axis',(-1.,0.,0.));
#25453=DIRECTION('ref_axis',(0.,-1.,5.55111512312578E-16));
#25454=DIRECTION('center_axis',(-1.,0.,0.));
#25455=DIRECTION('ref_axis',(0.,-1.,5.55111512312578E-16));
#25456=DIRECTION('center_axis',(1.,0.,0.));
#25457=DIRECTION('ref_axis',(0.,-1.,5.55111512312578E-16));
#25458=DIRECTION('center_axis',(1.,0.,0.));
#25459=DIRECTION('ref_axis',(0.,1.,2.77555756156289E-16));
#25460=DIRECTION('',(1.,0.,0.));
#25461=DIRECTION('center_axis',(1.,0.,0.));
#25462=DIRECTION('ref_axis',(0.,1.,2.77555756156289E-16));
#25463=DIRECTION('',(1.,0.,0.));
#25464=DIRECTION('center_axis',(0.,1.,0.));
#25465=DIRECTION('ref_axis',(0.,0.,1.));
#25466=DIRECTION('',(1.,0.,0.));
#25467=DIRECTION('',(0.,0.,-1.));
#25468=DIRECTION('center_axis',(1.,0.,0.));
#25469=DIRECTION('ref_axis',(0.,0.,-1.));
#25470=DIRECTION('center_axis',(1.,0.,0.));
#25471=DIRECTION('ref_axis',(0.,-1.,5.55111512312578E-16));
#25472=DIRECTION('',(1.,0.,0.));
#25473=DIRECTION('center_axis',(1.,0.,0.));
#25474=DIRECTION('ref_axis',(0.,-1.,5.55111512312578E-16));
#25475=DIRECTION('center_axis',(0.,-1.,0.));
#25476=DIRECTION('ref_axis',(0.,0.,-1.));
#25477=DIRECTION('',(0.,0.,1.));
#25478=DIRECTION('center_axis',(1.,0.,0.));
#25479=DIRECTION('ref_axis',(0.,0.,-1.));
#32185=CARTESIAN_POINT('',(0.,0.,0.));
#32186=CARTESIAN_POINT('Origin',(1.535,0.385,-1.2));
#32187=CARTESIAN_POINT('',(1.52,0.4,-0.6));
#32188=CARTESIAN_POINT('',(1.55,0.37,-0.6));
#32189=CARTESIAN_POINT('',(1.52,0.4,-0.6));
#32190=CARTESIAN_POINT('',(1.55,0.37,-1.4));
#32191=CARTESIAN_POINT('',(1.55,0.37,-1.2));
#32192=CARTESIAN_POINT('',(1.52,0.4,-1.4));
#32193=CARTESIAN_POINT('',(1.55,0.37,-1.4));
#32194=CARTESIAN_POINT('',(1.52,0.4,-1.2));
#32195=CARTESIAN_POINT('Origin',(1.535,2.77555756156289E-17,-0.6));
#32196=CARTESIAN_POINT('',(1.52,-0.4,-0.6));
#32197=CARTESIAN_POINT('',(1.55,-0.37,-0.6));
#32198=CARTESIAN_POINT('',(1.52,-0.4,-0.6));
#32199=CARTESIAN_POINT('Origin',(1.55,2.77555756156289E-17,-0.6));
#32200=CARTESIAN_POINT('Origin',(1.52,2.77555756156289E-17,-0.6));
#32201=CARTESIAN_POINT('Origin',(1.535,-0.385,-0.8));
#32202=CARTESIAN_POINT('',(1.52,-0.4,-1.4));
#32203=CARTESIAN_POINT('',(1.55,-0.37,-1.4));
#32204=CARTESIAN_POINT('',(1.52,-0.4,-1.4));
#32205=CARTESIAN_POINT('',(1.55,-0.37,-0.8));
#32206=CARTESIAN_POINT('',(1.52,-0.4,-0.8));
#32207=CARTESIAN_POINT('Origin',(1.535,2.77555756156289E-17,-1.4));
#32208=CARTESIAN_POINT('Origin',(1.55,2.77555756156289E-17,-1.4));
#32209=CARTESIAN_POINT('Origin',(1.52,2.77555756156289E-17,-1.4));
#32210=CARTESIAN_POINT('Origin',(0.85,2.77555756156289E-17,-0.6));
#32211=CARTESIAN_POINT('',(0.85,0.4,-0.6));
#32212=CARTESIAN_POINT('',(0.85,0.4,-0.6));
#32213=CARTESIAN_POINT('',(0.85,-0.4,-0.6));
#32214=CARTESIAN_POINT('Origin',(0.85,2.77555756156289E-17,-0.6));
#32215=CARTESIAN_POINT('',(0.85,-0.4,-0.6));
#32216=CARTESIAN_POINT('Origin',(0.85,0.4,-1.4));
#32217=CARTESIAN_POINT('',(0.85,0.4,-1.4));
#32218=CARTESIAN_POINT('',(0.85,0.4,-1.4));
#32219=CARTESIAN_POINT('',(0.85,0.4,-0.6));
#32220=CARTESIAN_POINT('Origin',(1.55,0.,-1.));
#32221=CARTESIAN_POINT('Origin',(0.85,2.77555756156289E-17,-1.4));
#32222=CARTESIAN_POINT('',(0.85,-0.4,-1.4));
#32223=CARTESIAN_POINT('',(0.85,-0.4,-1.4));
#32224=CARTESIAN_POINT('Origin',(0.85,2.77555756156289E-17,-1.4));
#32225=CARTESIAN_POINT('Origin',(0.85,-0.4,-0.6));
#32226=CARTESIAN_POINT('',(0.85,-0.4,-1.4));
#32227=CARTESIAN_POINT('Origin',(0.85,0.,-1.));
#59166=UNCERTAINTY_MEASURE_WITH_UNIT(LENGTH_MEASURE(0.001),#59205,
'DISTANCE_ACCURACY_VALUE',
'Maximum model space distance between geometric entities at asserted c
onnectivities');
#59182=UNCERTAINTY_MEASURE_WITH_UNIT(LENGTH_MEASURE(0.001),#59205,
'DISTANCE_ACCURACY_VALUE',
'Maximum model space distance between geometric entities at asserted c
onnectivities');
#59188=(
GEOMETRIC_REPRESENTATION_CONTEXT(3)
GLOBAL_UNCERTAINTY_ASSIGNED_CONTEXT((#59166))
GLOBAL_UNIT_ASSIGNED_CONTEXT((#59205,#59207,#59208))
REPRESENTATION_CONTEXT('','3D')
);
#59204=(
GEOMETRIC_REPRESENTATION_CONTEXT(3)
GLOBAL_UNCERTAINTY_ASSIGNED_CONTEXT((#59182))
GLOBAL_UNIT_ASSIGNED_CONTEXT((#59205,#59207,#59208))
REPRESENTATION_CONTEXT('','3D')
);
#59205=(
LENGTH_UNIT()
NAMED_UNIT(*)
SI_UNIT(.CENTI.,.METRE.)
);
#59207=(
NAMED_UNIT(*)
PLANE_ANGLE_UNIT()
SI_UNIT($,.RADIAN.)
);
#59208=(
NAMED_UNIT(*)
SI_UNIT($,.STERADIAN.)
SOLID_ANGLE_UNIT()
);
#59214=SHAPE_DEFINITION_REPRESENTATION(#59235,#59301);
#59235=PRODUCT_DEFINITION_SHAPE('',$,#59323);
#59301=SHAPE_REPRESENTATION('',(#23174),#59188);
#59317=PRODUCT_DEFINITION_CONTEXT('part definition',#59382,'design');
#59323=PRODUCT_DEFINITION('2026-10-23-00-47-21-965',
'16_DIN_6885_A_8x7x16_Parallel_Key',#59344,#59317);
#59344=PRODUCT_DEFINITION_FORMATION('',$,#59389);
#59382=APPLICATION_CONTEXT(
'Core Data for Automotive Mechanical Design Process');
#59383=PRODUCT_CONTEXT('part definition',#59382,'mechanical');
#59389=PRODUCT('2026-10-23-00-47-21-965',
'16_DIN_6885_A_8x7x16_Parallel_Key',$,(#59383));
#59580=COLOUR_RGB('Grey',0.48,0.52,0.57);
#59581=FILL_AREA_STYLE_COLOUR('',#59580);
#59582=FILL_AREA_STYLE('',(#59581));
#59583=SURFACE_STYLE_FILL_AREA(#59582);
#59584=SURFACE_SIDE_STYLE('',(#59583));
#59585=SURFACE_STYLE_USAGE(.BOTH.,#59584);
#59586=PRESENTATION_STYLE_ASSIGNMENT((#59585));
ENDSEC;
END-ISO-10303-21;
